ISO-10303-21;
HEADER;
/* Generated by software containing ST-Developer
 * from STEP Tools, Inc. (www.steptools.com) 
 */

FILE_DESCRIPTION(
/* description */ ('PAT-091'),
/* implementation_level */ '2;1');

FILE_NAME(
/* name */ 'Plain pivot bush (6).step',
/* time_stamp */ '2026-10-27T15:34:44-07:00',
/* author */ (''),
/* organization */ (''),
/* preprocessor_version */ 'ST-DEVELOPER v20.2',
/* originating_system */ 'Autodesk Translation Framework v15.17.0.0',
/* authorisation */ '');

FILE_SCHEMA (('AUTOMOTIVE_DESIGN { 1 0 10303 214 3 1 1 }'));
ENDSEC;

DATA;
#10=MECHANICAL_DESIGN_GEOMETRIC_PRESENTATION_REPRESENTATION('',(#1045),#25100);
#825=SHAPE_REPRESENTATION_RELATIONSHIP('SRR','None',#25592,#935);
#935=ADVANCED_BREP_SHAPE_REPRESENTATION('',(#1166),#25062);
#1045=STYLED_ITEM('',(#26177),#1166);
#1166=MANIFOLD_SOLID_BREP('Body1',#13325);
#1539=FACE_BOUND('',#3775,.T.);
#1540=FACE_BOUND('',#3777,.T.);
#1954=PLANE('',#15819);
#1955=PLANE('',#15820);
#2630=FACE_OUTER_BOUND('',#3772,.T.);
#2631=FACE_OUTER_BOUND('',#3773,.T.);
#2632=FACE_OUTER_BOUND('',#3774,.T.);
#2633=FACE_OUTER_BOUND('',#3776,.T.);
#3772=EDGE_LOOP('',(#11234,#11235,#11236,#11237));
#3773=EDGE_LOOP('',(#11238,#11239,#11240,#11241));
#3774=EDGE_LOOP('',(#11242));
#3775=EDGE_LOOP('',(#11243));
#3776=EDGE_LOOP('',(#11244));
#3777=EDGE_LOOP('',(#11245));
#4747=LINE('',#23635,#5487);
#4748=LINE('',#23641,#5488);
#5487=VECTOR('',#19551,0.604999999999997);
#5488=VECTOR('',#19558,1.);
#6108=CIRCLE('',#15814,0.604999999999997);
#6109=CIRCLE('',#15815,0.604999999999997);
#6110=CIRCLE('',#15817,1.);
#6111=CIRCLE('',#15818,1.);
#7133=VERTEX_POINT('',#23632);
#7134=VERTEX_POINT('',#23634);
#7135=VERTEX_POINT('',#23638);
#7136=VERTEX_POINT('',#23640);
#8552=EDGE_CURVE('',#7133,#7133,#6108,.T.);
#8553=EDGE_CURVE('',#7133,#7134,#4747,.T.);
#8554=EDGE_CURVE('',#7134,#7134,#6109,.T.);
#8555=EDGE_CURVE('',#7135,#7135,#6110,.T.);
#8556=EDGE_CURVE('',#7135,#7136,#4748,.T.);
#8557=EDGE_CURVE('',#7136,#7136,#6111,.T.);
#11234=ORIENTED_EDGE('',*,*,#8552,.F.);
#11235=ORIENTED_EDGE('',*,*,#8553,.T.);
#11236=ORIENTED_EDGE('',*,*,#8554,.T.);
#11237=ORIENTED_EDGE('',*,*,#8553,.F.);
#11238=ORIENTED_EDGE('',*,*,#8555,.F.);
#11239=ORIENTED_EDGE('',*,*,#8556,.T.);
#11240=ORIENTED_EDGE('',*,*,#8557,.T.);
#11241=ORIENTED_EDGE('',*,*,#8556,.F.);
#11242=ORIENTED_EDGE('',*,*,#8555,.T.);
#11243=ORIENTED_EDGE('',*,*,#8552,.T.);
#11244=ORIENTED_EDGE('',*,*,#8557,.F.);
#11245=ORIENTED_EDGE('',*,*,#8554,.F.);
#12315=CYLINDRICAL_SURFACE('',#15813,0.604999999999997);
#12316=CYLINDRICAL_SURFACE('',#15816,1.);
#12997=ADVANCED_FACE('',(#2630),#12315,.F.);
#12998=ADVANCED_FACE('',(#2631),#12316,.T.);
#12999=ADVANCED_FACE('',(#2632,#1539),#1954,.T.);
#13000=ADVANCED_FACE('',(#2633,#1540),#1955,.F.);
#13325=CLOSED_SHELL('',(#12997,#12998,#12999,#13000));
#15812=AXIS2_PLACEMENT_3D('',#23630,#19545,#19546);
#15813=AXIS2_PLACEMENT_3D('',#23631,#19547,#19548);
#15814=AXIS2_PLACEMENT_3D('',#23633,#19549,#19550);
#15815=AXIS2_PLACEMENT_3D('',#23636,#19552,#19553);
#15816=AXIS2_PLACEMENT_3D('',#23637,#19554,#19555);
#15817=AXIS2_PLACEMENT_3D('',#23639,#19556,#19557);
#15818=AXIS2_PLACEMENT_3D('',#23642,#19559,#19560);
#15819=AXIS2_PLACEMENT_3D('',#23643,#19561,#19562);
#15820=AXIS2_PLACEMENT_3D('',#23644,#19563,#19564);
#19545=DIRECTION('axis',(0.,0.,1.));
#19546=DIRECTION('refdir',(1.,0.,0.));
#19547=DIRECTION('center_axis',(0.,1.,0.));
#19548=DIRECTION('ref_axis',(1.,0.,0.));
#19549=DIRECTION('center_axis',(0.,-1.,0.));
#19550=DIRECTION('ref_axis',(1.,0.,0.));
#19551=DIRECTION('',(0.,-1.,0.));
#19552=DIRECTION('center_axis',(0.,-1.,0.));
#19553=DIRECTION('ref_axis',(1.,0.,0.));
#19554=DIRECTION('center_axis',(0.,1.,0.));
#19555=DIRECTION('ref_axis',(1.,0.,0.));
#19556=DIRECTION('center_axis',(0.,1.,0.));
#19557=DIRECTION('ref_axis',(1.,0.,0.));
#19558=DIRECTION('',(0.,-1.,0.));
#19559=DIRECTION('center_axis',(0.,1.,0.));
#19560=DIRECTION('ref_axis',(1.,0.,0.));
#19561=DIRECTION('center_axis',(0.,1.,0.));
#19562=DIRECTION('ref_axis',(1.,0.,0.));
#19563=DIRECTION('center_axis',(0.,1.,0.));
#19564=DIRECTION('ref_axis',(1.,0.,0.));
#23630=CARTESIAN_POINT('',(0.,0.,0.));
#23631=CARTESIAN_POINT('Origin',(38.7298334620742,-5.5,3.));
#23632=CARTESIAN_POINT('',(38.1248334620742,-4.5,3.));
#23633=CARTESIAN_POINT('Origin',(38.7298334620742,-4.5,3.));
#23634=CARTESIAN_POINT('',(38.1248334620742,-5.5,3.));
#23635=CARTESIAN_POINT('',(38.1248334620742,-5.5,3.));
#23636=CARTESIAN_POINT('Origin',(38.7298334620742,-5.5,3.));
#23637=CARTESIAN_POINT('Origin',(38.7298334620742,-5.5,3.));
#23638=CARTESIAN_POINT('',(37.7298334620742,-4.5,3.));
#23639=CARTESIAN_POINT('Origin',(38.7298334620742,-4.5,3.));
#23640=CARTESIAN_POINT('',(37.7298334620742,-5.5,3.));
#23641=CARTESIAN_POINT('',(37.7298334620742,-5.5,3.));
#23642=CARTESIAN_POINT('Origin',(38.7298334620742,-5.5,3.));
#23643=CARTESIAN_POINT('Origin',(38.7298334620742,-4.5,3.));
#23644=CARTESIAN_POINT('Origin',(38.7298334620742,-5.5,3.));
#24941=UNCERTAINTY_MEASURE_WITH_UNIT(LENGTH_MEASURE(0.001),#25101,
'DISTANCE_ACCURACY_VALUE',
'Maximum model space distance between geometric entities at asserted c
onnectivities');
#24979=UNCERTAINTY_MEASURE_WITH_UNIT(LENGTH_MEASURE(0.001),#25101,
'DISTANCE_ACCURACY_VALUE',
'Maximum model space distance between geometric entities at asserted c
onnectivities');
#25062=(
GEOMETRIC_REPRESENTATION_CONTEXT(3)
GLOBAL_UNCERTAINTY_ASSIGNED_CONTEXT((#24941))
GLOBAL_UNIT_ASSIGNED_CONTEXT((#25101,#25103,#25104))
REPRESENTATION_CONTEXT('','3D')
);
#25100=(
GEOMETRIC_REPRESENTATION_CONTEXT(3)
GLOBAL_UNCERTAINTY_ASSIGNED_CONTEXT((#24979))
GLOBAL_UNIT_ASSIGNED_CONTEXT((#25101,#25103,#25104))
REPRESENTATION_CONTEXT('','3D')
);
#25101=(
LENGTH_UNIT()
NAMED_UNIT(*)
SI_UNIT(.CENTI.,.METRE.)
);
#25103=(
NAMED_UNIT(*)
PLANE_ANGLE_UNIT()
SI_UNIT($,.RADIAN.)
);
#25104=(
NAMED_UNIT(*)
SI_UNIT($,.STERADIAN.)
SOLID_ANGLE_UNIT()
);
#25187=SHAPE_DEFINITION_REPRESENTATION(#25381,#25592);
#25381=PRODUCT_DEFINITION_SHAPE('',$,#25713);
#25592=SHAPE_REPRESENTATION('',(#15812),#25062);
#25630=PRODUCT_DEFINITION_CONTEXT('part definition',#25992,'design');
#25713=PRODUCT_DEFINITION('Plain pivot bush (6)','Plain pivot bush (6)',#25833,
#25630);
#25833=PRODUCT_DEFINITION_FORMATION('',$,#26076);
#25992=APPLICATION_CONTEXT(
'Core Data for Automotive Mechanical Design Process');
#25993=PRODUCT_CONTEXT('part definition',#25992,'mechanical');
#26076=PRODUCT('Plain pivot bush (6)','Plain pivot bush (6)',
'Plain pivot bush (6)',(#25993));
#26171=COLOUR_RGB('Light Blue',0.38,0.62,0.78);
#26172=FILL_AREA_STYLE_COLOUR('',#26171);
#26173=FILL_AREA_STYLE('',(#26172));
#26174=SURFACE_STYLE_FILL_AREA(#26173);
#26175=SURFACE_SIDE_STYLE('',(#26174));
#26176=SURFACE_STYLE_USAGE(.BOTH.,#26175);
#26177=PRESENTATION_STYLE_ASSIGNMENT((#26176));
ENDSEC;
END-ISO-10303-21;
